ISO-10303-21;
HEADER;
/* Generated by software containing ST-Developer
 * from STEP Tools, Inc. (www.steptools.com) 
 */

FILE_DESCRIPTION(
/* description */ ('Lever-operated bar clamp (toggle)'),
/* implementation_level */ '2;1');

FILE_NAME(
/* name */ 'Link bush (1).step',
/* time_stamp */ '2026-10-28T03:25:02-07:00',
/* author */ (''),
/* organization */ (''),
/* preprocessor_version */ 'ST-DEVELOPER v20.2',
/* originating_system */ 'Autodesk Translation Framework v15.17.0.0',
/* authorisation */ '');

FILE_SCHEMA (('AUTOMOTIVE_DESIGN { 1 0 10303 214 3 1 1 }'));
ENDSEC;

DATA;
#10=MECHANICAL_DESIGN_GEOMETRIC_PRESENTATION_REPRESENTATION('',(#451),#12413);
#367=SHAPE_REPRESENTATION_RELATIONSHIP('SRR','None',#12610,#405);
#405=ADVANCED_BREP_SHAPE_REPRESENTATION('',(#494),#12407);
#451=STYLED_ITEM('',(#12883),#494);
#494=MANIFOLD_SOLID_BREP('Body1',#6614);
#642=FACE_BOUND('',#1797,.T.);
#643=FACE_BOUND('',#1799,.T.);
#853=PLANE('',#7807);
#854=PLANE('',#7808);
#1246=FACE_OUTER_BOUND('',#1794,.T.);
#1247=FACE_OUTER_BOUND('',#1795,.T.);
#1248=FACE_OUTER_BOUND('',#1796,.T.);
#1249=FACE_OUTER_BOUND('',#1798,.T.);
#1794=EDGE_LOOP('',(#5841,#5842,#5843,#5844));
#1795=EDGE_LOOP('',(#5845,#5846,#5847,#5848));
#1796=EDGE_LOOP('',(#5849));
#1797=EDGE_LOOP('',(#5850));
#1798=EDGE_LOOP('',(#5851));
#1799=EDGE_LOOP('',(#5852));
#2227=LINE('',#12085,#2668);
#2228=LINE('',#12091,#2669);
#2668=VECTOR('',#9798,0.305);
#2669=VECTOR('',#9805,0.5);
#3045=CIRCLE('',#7802,0.305);
#3046=CIRCLE('',#7803,0.305);
#3047=CIRCLE('',#7805,0.5);
#3048=CIRCLE('',#7806,0.5);
#3552=VERTEX_POINT('',#12082);
#3553=VERTEX_POINT('',#12084);
#3554=VERTEX_POINT('',#12088);
#3555=VERTEX_POINT('',#12090);
#4325=EDGE_CURVE('',#3552,#3552,#3045,.T.);
#4326=EDGE_CURVE('',#3552,#3553,#2227,.T.);
#4327=EDGE_CURVE('',#3553,#3553,#3046,.T.);
#4328=EDGE_CURVE('',#3554,#3554,#3047,.T.);
#4329=EDGE_CURVE('',#3554,#3555,#2228,.T.);
#4330=EDGE_CURVE('',#3555,#3555,#3048,.T.);
#5841=ORIENTED_EDGE('',*,*,#4325,.F.);
#5842=ORIENTED_EDGE('',*,*,#4326,.T.);
#5843=ORIENTED_EDGE('',*,*,#4327,.T.);
#5844=ORIENTED_EDGE('',*,*,#4326,.F.);
#5845=ORIENTED_EDGE('',*,*,#4328,.F.);
#5846=ORIENTED_EDGE('',*,*,#4329,.T.);
#5847=ORIENTED_EDGE('',*,*,#4330,.T.);
#5848=ORIENTED_EDGE('',*,*,#4329,.F.);
#5849=ORIENTED_EDGE('',*,*,#4328,.T.);
#5850=ORIENTED_EDGE('',*,*,#4325,.T.);
#5851=ORIENTED_EDGE('',*,*,#4330,.F.);
#5852=ORIENTED_EDGE('',*,*,#4327,.F.);
#6152=CYLINDRICAL_SURFACE('',#7801,0.305);
#6153=CYLINDRICAL_SURFACE('',#7804,0.5);
#6521=ADVANCED_FACE('',(#1246),#6152,.F.);
#6522=ADVANCED_FACE('',(#1247),#6153,.T.);
#6523=ADVANCED_FACE('',(#1248,#642),#853,.T.);
#6524=ADVANCED_FACE('',(#1249,#643),#854,.F.);
#6614=CLOSED_SHELL('',(#6521,#6522,#6523,#6524));
#7800=AXIS2_PLACEMENT_3D('',#12080,#9792,#9793);
#7801=AXIS2_PLACEMENT_3D('',#12081,#9794,#9795);
#7802=AXIS2_PLACEMENT_3D('',#12083,#9796,#9797);
#7803=AXIS2_PLACEMENT_3D('',#12086,#9799,#9800);
#7804=AXIS2_PLACEMENT_3D('',#12087,#9801,#9802);
#7805=AXIS2_PLACEMENT_3D('',#12089,#9803,#9804);
#7806=AXIS2_PLACEMENT_3D('',#12092,#9806,#9807);
#7807=AXIS2_PLACEMENT_3D('',#12093,#9808,#9809);
#7808=AXIS2_PLACEMENT_3D('',#12094,#9810,#9811);
#9792=DIRECTION('axis',(0.,0.,1.));
#9793=DIRECTION('refdir',(1.,0.,0.));
#9794=DIRECTION('center_axis',(0.,1.,0.));
#9795=DIRECTION('ref_axis',(1.,0.,0.));
#9796=DIRECTION('center_axis',(0.,-1.,0.));
#9797=DIRECTION('ref_axis',(1.,0.,0.));
#9798=DIRECTION('',(0.,-1.,0.));
#9799=DIRECTION('center_axis',(0.,-1.,0.));
#9800=DIRECTION('ref_axis',(1.,0.,0.));
#9801=DIRECTION('center_axis',(0.,1.,0.));
#9802=DIRECTION('ref_axis',(1.,0.,0.));
#9803=DIRECTION('center_axis',(0.,1.,0.));
#9804=DIRECTION('ref_axis',(1.,0.,0.));
#9805=DIRECTION('',(0.,-1.,0.));
#9806=DIRECTION('center_axis',(0.,1.,0.));
#9807=DIRECTION('ref_axis',(1.,0.,0.));
#9808=DIRECTION('center_axis',(0.,1.,0.));
#9809=DIRECTION('ref_axis',(1.,0.,0.));
#9810=DIRECTION('center_axis',(0.,1.,0.));
#9811=DIRECTION('ref_axis',(1.,0.,0.));
#12080=CARTESIAN_POINT('',(0.,0.,0.));
#12081=CARTESIAN_POINT('Origin',(0.,-5.5,4.668081457105));
#12082=CARTESIAN_POINT('',(-0.305,-4.7,4.668081457105));
#12083=CARTESIAN_POINT('Origin',(0.,-4.7,4.668081457105));
#12084=CARTESIAN_POINT('',(-0.305,-5.5,4.668081457105));
#12085=CARTESIAN_POINT('',(-0.305,-5.5,4.668081457105));
#12086=CARTESIAN_POINT('Origin',(0.,-5.5,4.668081457105));
#12087=CARTESIAN_POINT('Origin',(0.,-5.5,4.668081457105));
#12088=CARTESIAN_POINT('',(-0.5,-4.7,4.668081457105));
#12089=CARTESIAN_POINT('Origin',(0.,-4.7,4.668081457105));
#12090=CARTESIAN_POINT('',(-0.5,-5.5,4.668081457105));
#12091=CARTESIAN_POINT('',(-0.5,-5.5,4.668081457105));
#12092=CARTESIAN_POINT('Origin',(0.,-5.5,4.668081457105));
#12093=CARTESIAN_POINT('Origin',(0.,-4.7,4.668081457105));
#12094=CARTESIAN_POINT('Origin',(0.,-5.5,4.668081457105));
#12361=UNCERTAINTY_MEASURE_WITH_UNIT(LENGTH_MEASURE(0.001),#12414,
'DISTANCE_ACCURACY_VALUE',
'Maximum model space distance between geometric entities at asserted c
onnectivities');
#12367=UNCERTAINTY_MEASURE_WITH_UNIT(LENGTH_MEASURE(0.001),#12414,
'DISTANCE_ACCURACY_VALUE',
'Maximum model space distance between geometric entities at asserted c
onnectivities');
#12407=(
GEOMETRIC_REPRESENTATION_CONTEXT(3)
GLOBAL_UNCERTAINTY_ASSIGNED_CONTEXT((#12361))
GLOBAL_UNIT_ASSIGNED_CONTEXT((#12414,#12416,#12417))
REPRESENTATION_CONTEXT('','3D')
);
#12413=(
GEOMETRIC_REPRESENTATION_CONTEXT(3)
GLOBAL_UNCERTAINTY_ASSIGNED_CONTEXT((#12367))
GLOBAL_UNIT_ASSIGNED_CONTEXT((#12414,#12416,#12417))
REPRESENTATION_CONTEXT('','3D')
);
#12414=(
LENGTH_UNIT()
NAMED_UNIT(*)
SI_UNIT(.CENTI.,.METRE.)
);
#12416=(
NAMED_UNIT(*)
PLANE_ANGLE_UNIT()
SI_UNIT($,.RADIAN.)
);
#12417=(
NAMED_UNIT(*)
SI_UNIT($,.STERADIAN.)
SOLID_ANGLE_UNIT()
);
#12457=SHAPE_DEFINITION_REPRESENTATION(#12554,#12610);
#12554=PRODUCT_DEFINITION_SHAPE('',$,#12656);
#12610=SHAPE_REPRESENTATION('',(#7800),#12407);
#12616=PRODUCT_DEFINITION_CONTEXT('part definition',#12753,'design');
#12656=PRODUCT_DEFINITION('Link bush (1)','Link bush (1)',#12701,#12616);
#12701=PRODUCT_DEFINITION_FORMATION('',$,#12794);
#12753=APPLICATION_CONTEXT(
'Core Data for Automotive Mechanical Design Process');
#12754=PRODUCT_CONTEXT('part definition',#12753,'mechanical');
#12794=PRODUCT('Link bush (1)','Link bush (1)','Link bush (1)',(#12754));
#12877=COLOUR_RGB('Off White',0.89,0.88,0.83);
#12878=FILL_AREA_STYLE_COLOUR('',#12877);
#12879=FILL_AREA_STYLE('',(#12878));
#12880=SURFACE_STYLE_FILL_AREA(#12879);
#12881=SURFACE_SIDE_STYLE('',(#12880));
#12882=SURFACE_STYLE_USAGE(.BOTH.,#12881);
#12883=PRESENTATION_STYLE_ASSIGNMENT((#12882));
ENDSEC;
END-ISO-10303-21;
